ISO-10303-21;
HEADER;
/* Generated by software containing ST-Developer
 * from STEP Tools, Inc. (www.steptools.com) 
 */

FILE_DESCRIPTION(
/* description */ ('STEP AP214'),
/* implementation_level */ '2;1');

FILE_NAME(
/* name */ 'screw driver.step',
/* time_stamp */ '2026-11-04T19:14:12-08:00',
/* author */ (''),
/* organization */ (''),
/* preprocessor_version */ 'ST-DEVELOPER v20.2',
/* originating_system */ 'Autodesk Translation Framework v15.17.0.0',
/* authorisation */ '');

FILE_SCHEMA (('AUTOMOTIVE_DESIGN { 1 0 10303 214 3 1 1 }'));
ENDSEC;

DATA;
#10=MECHANICAL_DESIGN_GEOMETRIC_PRESENTATION_REPRESENTATION('',(#103),#5990);
#47=(
BOUNDED_SURFACE()
B_SPLINE_SURFACE(3,2,((#5769,#5770,#5771),(#5772,#5773,#5774),(#5775,#5776,
#5777),(#5778,#5779,#5780),(#5781,#5782,#5783),(#5784,#5785,#5786),(#5787,
#5788,#5789),(#5790,#5791,#5792),(#5793,#5794,#5795),(#5796,#5797,#5798),
(#5799,#5800,#5801),(#5802,#5803,#5804),(#5805,#5806,#5807),(#5808,#5809,
#5810),(#5811,#5812,#5813),(#5814,#5815,#5816),(#5817,#5818,#5819),(#5820,
#5821,#5822)),.UNSPECIFIED.,.F.,.F.,.F.)
B_SPLINE_SURFACE_WITH_KNOTS((4,2,2,2,2,2,2,2,4),(3,3),(0.00467154358091484,
0.00499795425216117,0.00521234917938639,0.00542674410661162,0.00564113903383685,
0.00585553396106207,0.0060699288882873,0.00628432381551252,0.00661073448675885),
(0.,1.00011201574402),.UNSPECIFIED.)
GEOMETRIC_REPRESENTATION_ITEM()
RATIONAL_B_SPLINE_SURFACE(((1.,0.701778016251575,1.00006681111479),(1.,
0.706507936356085,1.00006575146375),(1.,0.712393708374132,1.00006443286548),
(1.,0.724799452378116,1.00006165358819),(1.,0.730457055067376,1.00006038610704),
(1.,0.742658843750505,1.00005765252217),(1.,0.749286323952398,1.00005616775792),
(1.,0.759971140951244,1.00005377402247),(1.,0.763704964258696,1.00005293752847),
(1.,0.763766920917064,1.00005292364823),(1.,0.760086272902725,1.00005374822928),
(1.,0.74942657380375,1.00005613633753),(1.,0.742780641856394,1.00005762523556),
(1.,0.730540791311145,1.00006036734749),(1.,0.724865847327457,1.00006163871363),
(1.,0.712422254236158,1.00006442647031),(1.,0.706506681063795,1.00006575174497),
(1.,0.701749277073212,1.00006681755327)))
REPRESENTATION_ITEM('')
SURFACE()
);
#48=(
BOUNDED_SURFACE()
B_SPLINE_SURFACE(3,2,((#5827,#5828,#5829),(#5830,#5831,#5832),(#5833,#5834,
#5835),(#5836,#5837,#5838),(#5839,#5840,#5841),(#5842,#5843,#5844),(#5845,
#5846,#5847),(#5848,#5849,#5850),(#5851,#5852,#5853),(#5854,#5855,#5856),
(#5857,#5858,#5859),(#5860,#5861,#5862),(#5863,#5864,#5865),(#5866,#5867,
#5868),(#5869,#5870,#5871),(#5872,#5873,#5874),(#5875,#5876,#5877),(#5878,
#5879,#5880)),.UNSPECIFIED.,.F.,.F.,.F.)
B_SPLINE_SURFACE_WITH_KNOTS((4,2,2,2,2,2,2,2,4),(3,3),(0.00467154358091712,
0.00499795425216117,0.0052123491793864,0.00542674410661162,0.00564113903383685,
0.00585553396106207,0.0060699288882873,0.00628432381551253,0.00661073448675658),
(0.,1.00011201574402),.UNSPECIFIED.)
GEOMETRIC_REPRESENTATION_ITEM()
RATIONAL_B_SPLINE_SURFACE(((1.,0.701778016251691,1.00006681111478),(1.,
0.706507936356154,1.00006575146375),(1.,0.712393708374192,1.00006443286548),
(1.,0.724799452378113,1.00006165358819),(1.,0.730457055067361,1.00006038610704),
(1.,0.742658843750522,1.00005765252217),(1.,0.749286323952399,1.00005616775792),
(1.,0.759971140951245,1.00005377402246),(1.,0.763704964258696,1.00005293752847),
(1.,0.763766920917065,1.00005292364823),(1.,0.760086272902701,1.00005374822928),
(1.,0.749426573803775,1.00005613633753),(1.,0.742780641856403,1.00005762523556),
(1.,0.730540791311137,1.00006036734749),(1.,0.724865847327466,1.00006163871363),
(1.,0.712422254236199,1.00006442647031),(1.,0.706506681063906,1.00006575174497),
(1.,0.70174927707328,1.00006681755327)))
REPRESENTATION_ITEM('')
SURFACE()
);
#71=B_SPLINE_CURVE_WITH_KNOTS('',3,(#5643,#5644,#5645,#5646,#5647,#5648,
#5649,#5650,#5651,#5652,#5653,#5654,#5655,#5656,#5657,#5658,#5659,#5660,
#5661,#5662,#5663,#5664,#5665,#5666,#5667),.UNSPECIFIED.,.F.,.F.,(4,3,3,
3,3,3,3,3,4),(0.,0.000216694552239529,0.00043295736495498,0.000650463962575776,
0.00086591472990996,0.00108361531562917,0.00129887209486494,0.00151612908143691,
0.00173182945981992),.UNSPECIFIED.);
#72=B_SPLINE_CURVE_WITH_KNOTS('',3,(#5680,#5681,#5682,#5683,#5684,#5685,
#5686,#5687,#5688,#5689,#5690,#5691,#5692,#5693,#5694,#5695,#5696,#5697,
#5698,#5699,#5700,#5701,#5702,#5703,#5704),.UNSPECIFIED.,.F.,.F.,(4,3,3,
3,3,3,3,3,4),(0.,0.000216694552239523,0.00043295736495498,0.000650463962575778,
0.00086591472990996,0.00108361531562917,0.00129887209486494,0.00151612908143692,
0.00173182945981992),.UNSPECIFIED.);
#89=SHAPE_REPRESENTATION_RELATIONSHIP('SRR','None',#6025,#96);
#96=ADVANCED_BREP_SHAPE_REPRESENTATION('',(#110),#5987);
#103=STYLED_ITEM('',(#6067),#110);
#110=MANIFOLD_SOLID_BREP('Body1',#3273);
#131=FACE_BOUND('',#577,.T.);
#132=FACE_BOUND('',#579,.T.);
#212=PLANE('',#3602);
#213=PLANE('',#3603);
#214=PLANE('',#3604);
#215=PLANE('',#3605);
#216=PLANE('',#3606);
#217=PLANE('',#3607);
#218=PLANE('',#3608);
#219=PLANE('',#3612);
#220=PLANE('',#3616);
#221=PLANE('',#3617);
#222=PLANE('',#3618);
#223=PLANE('',#3619);
#224=PLANE('',#3620);
#225=PLANE('',#3621);
#226=PLANE('',#3622);
#227=PLANE('',#3623);
#228=PLANE('',#3624);
#229=PLANE('',#3625);
#230=PLANE('',#3626);
#231=PLANE('',#3627);
#232=PLANE('',#3628);
#372=FACE_OUTER_BOUND('',#568,.T.);
#373=FACE_OUTER_BOUND('',#569,.T.);
#374=FACE_OUTER_BOUND('',#570,.T.);
#375=FACE_OUTER_BOUND('',#571,.T.);
#376=FACE_OUTER_BOUND('',#572,.T.);
#377=FACE_OUTER_BOUND('',#573,.T.);
#378=FACE_OUTER_BOUND('',#574,.T.);
#379=FACE_OUTER_BOUND('',#575,.T.);
#380=FACE_OUTER_BOUND('',#576,.T.);
#381=FACE_OUTER_BOUND('',#578,.T.);
#382=FACE_OUTER_BOUND('',#580,.T.);
#383=FACE_OUTER_BOUND('',#581,.T.);
#384=FACE_OUTER_BOUND('',#582,.T.);
#385=FACE_OUTER_BOUND('',#583,.T.);
#386=FACE_OUTER_BOUND('',#584,.T.);
#387=FACE_OUTER_BOUND('',#585,.T.);
#388=FACE_OUTER_BOUND('',#586,.T.);
#389=FACE_OUTER_BOUND('',#587,.T.);
#390=FACE_OUTER_BOUND('',#588,.T.);
#391=FACE_OUTER_BOUND('',#589,.T.);
#392=FACE_OUTER_BOUND('',#590,.T.);
#393=FACE_OUTER_BOUND('',#591,.T.);
#394=FACE_OUTER_BOUND('',#592,.T.);
#395=FACE_OUTER_BOUND('',#593,.T.);
#396=FACE_OUTER_BOUND('',#594,.T.);
#397=FACE_OUTER_BOUND('',#595,.T.);
#398=FACE_OUTER_BOUND('',#596,.T.);
#399=FACE_OUTER_BOUND('',#597,.T.);
#400=FACE_OUTER_BOUND('',#598,.T.);
#401=FACE_OUTER_BOUND('',#599,.T.);
#568=EDGE_LOOP('',(#2816,#2817,#2818,#2819));
#569=EDGE_LOOP('',(#2820,#2821,#2822,#2823,#2824,#2825,#2826,#2827,#2828,
#2829,#2830,#2831,#2832,#2833));
#570=EDGE_LOOP('',(#2834,#2835,#2836));
#571=EDGE_LOOP('',(#2837,#2838,#2839));
#572=EDGE_LOOP('',(#2840,#2841,#2842));
#573=EDGE_LOOP('',(#2843,#2844,#2845,#2846,#2847,#2848));
#574=EDGE_LOOP('',(#2849,#2850,#2851,#2852,#2853,#2854));
#575=EDGE_LOOP('',(#2855,#2856,#2857));
#576=EDGE_LOOP('',(#2858,#2859,#2860,#2861,#2862,#2863,#2864));
#577=EDGE_LOOP('',(#2865));
#578=EDGE_LOOP('',(#2866,#2867,#2868,#2869,#2870,#2871,#2872));
#579=EDGE_LOOP('',(#2873));
#580=EDGE_LOOP('',(#2874,#2875,#2876,#2877,#2878));
#581=EDGE_LOOP('',(#2879,#2880,#2881,#2882,#2883));
#582=EDGE_LOOP('',(#2884,#2885,#2886,#2887,#2888));
#583=EDGE_LOOP('',(#2889,#2890,#2891,#2892,#2893));
#584=EDGE_LOOP('',(#2894,#2895,#2896,#2897,#2898));
#585=EDGE_LOOP('',(#2899,#2900,#2901,#2902,#2903));
#586=EDGE_LOOP('',(#2904,#2905,#2906));
#587=EDGE_LOOP('',(#2907,#2908,#2909));
#588=EDGE_LOOP('',(#2910,#2911,#2912));
#589=EDGE_LOOP('',(#2913,#2914,#2915));
#590=EDGE_LOOP('',(#2916,#2917,#2918));
#591=EDGE_LOOP('',(#2919,#2920,#2921));
#592=EDGE_LOOP('',(#2922,#2923,#2924,#2925,#2926,#2927));
#593=EDGE_LOOP('',(#2928,#2929,#2930,#2931));
#594=EDGE_LOOP('',(#2932,#2933,#2934,#2935));
#595=EDGE_LOOP('',(#2936,#2937,#2938,#2939));
#596=EDGE_LOOP('',(#2940,#2941,#2942,#2943));
#597=EDGE_LOOP('',(#2944,#2945,#2946,#2947));
#598=EDGE_LOOP('',(#2948,#2949,#2950,#2951));
#599=EDGE_LOOP('',(#2952,#2953,#2954,#2955));
#863=LINE('',#5592,#1166);
#864=LINE('',#5603,#1167);
#865=LINE('',#5622,#1168);
#866=LINE('',#5623,#1169);
#867=LINE('',#5626,#1170);
#868=LINE('',#5627,#1171);
#869=LINE('',#5630,#1172);
#870=LINE('',#5631,#1173);
#871=LINE('',#5635,#1174);
#872=LINE('',#5637,#1175);
#873=LINE('',#5639,#1176);
#874=LINE('',#5641,#1177);
#875=LINE('',#5668,#1178);
#876=LINE('',#5672,#1179);
#877=LINE('',#5674,#1180);
#878=LINE('',#5676,#1181);
#879=LINE('',#5678,#1182);
#880=LINE('',#5705,#1183);
#881=LINE('',#5708,#1184);
#882=LINE('',#5709,#1185);
#883=LINE('',#5720,#1186);
#884=LINE('',#5722,#1187);
#885=LINE('',#5724,#1188);
#886=LINE('',#5726,#1189);
#887=LINE('',#5727,#1190);
#888=LINE('',#5730,#1191);
#889=LINE('',#5731,#1192);
#890=LINE('',#5733,#1193);
#891=LINE('',#5734,#1194);
#892=LINE('',#5737,#1195);
#893=LINE('',#5738,#1196);
#894=LINE('',#5740,#1197);
#895=LINE('',#5741,#1198);
#896=LINE('',#5744,#1199);
#897=LINE('',#5745,#1200);
#898=LINE('',#5747,#1201);
#899=LINE('',#5748,#1202);
#900=LINE('',#5751,#1203);
#901=LINE('',#5752,#1204);
#902=LINE('',#5754,#1205);
#903=LINE('',#5755,#1206);
#904=LINE('',#5757,#1207);
#905=LINE('',#5758,#1208);
#906=LINE('',#5759,#1209);
#1166=VECTOR('',#4394,2.);
#1167=VECTOR('',#4405,1.);
#1168=VECTOR('',#4426,1000.);
#1169=VECTOR('',#4427,1000.);
#1170=VECTOR('',#4430,1000.);
#1171=VECTOR('',#4431,1000.);
#1172=VECTOR('',#4434,1000.);
#1173=VECTOR('',#4435,1000.);
#1174=VECTOR('',#4438,1000.);
#1175=VECTOR('',#4439,1000.);
#1176=VECTOR('',#4440,1000.);
#1177=VECTOR('',#4441,1000.);
#1178=VECTOR('',#4442,1000.);
#1179=VECTOR('',#4445,1000.);
#1180=VECTOR('',#4446,1000.);
#1181=VECTOR('',#4447,1000.);
#1182=VECTOR('',#4448,1000.);
#1183=VECTOR('',#4449,1000.);
#1184=VECTOR('',#4452,1000.);
#1185=VECTOR('',#4453,1000.);
#1186=VECTOR('',#4472,1000.);
#1187=VECTOR('',#4473,1000.);
#1188=VECTOR('',#4474,1000.);
#1189=VECTOR('',#4475,1000.);
#1190=VECTOR('',#4476,1000.);
#1191=VECTOR('',#4479,1000.);
#1192=VECTOR('',#4480,1000.);
#1193=VECTOR('',#4481,1000.);
#1194=VECTOR('',#4482,1000.);
#1195=VECTOR('',#4485,1000.);
#1196=VECTOR('',#4486,1000.);
#1197=VECTOR('',#4487,1000.);
#1198=VECTOR('',#4488,1000.);
#1199=VECTOR('',#4491,1000.);
#1200=VECTOR('',#4492,1000.);
#1201=VECTOR('',#4493,1000.);
#1202=VECTOR('',#4494,1000.);
#1203=VECTOR('',#4497,1000.);
#1204=VECTOR('',#4498,1000.);
#1205=VECTOR('',#4499,1000.);
#1206=VECTOR('',#4500,1000.);
#1207=VECTOR('',#4503,1000.);
#1208=VECTOR('',#4504,1000.);
#1209=VECTOR('',#4505,1000.);
#1314=CIRCLE('',#3587,2.);
#1315=CIRCLE('',#3588,2.);
#1316=CIRCLE('',#3590,1.);
#1317=CIRCLE('',#3591,1.);
#1318=CIRCLE('',#3592,1.);
#1319=CIRCLE('',#3593,1.);
#1320=CIRCLE('',#3594,1.);
#1321=CIRCLE('',#3595,1.);
#1322=CIRCLE('',#3596,1.);
#1323=CIRCLE('',#3597,1.);
#1324=CIRCLE('',#3598,1.);
#1325=CIRCLE('',#3599,1.);
#1326=CIRCLE('',#3600,1.);
#1327=CIRCLE('',#3601,1.);
#1328=CIRCLE('',#3609,3.5);
#1329=CIRCLE('',#3610,3.);
#1330=CIRCLE('',#3611,3.);
#1331=CIRCLE('',#3613,3.5);
#1332=CIRCLE('',#3614,3.);
#1333=CIRCLE('',#3615,3.);
#1334=CIRCLE('',#3630,3.);
#1335=CIRCLE('',#3631,3.);
#1336=CIRCLE('',#3634,3.);
#1337=CIRCLE('',#3635,3.);
#1585=VERTEX_POINT('',#5589);
#1586=VERTEX_POINT('',#5591);
#1587=VERTEX_POINT('',#5595);
#1588=VERTEX_POINT('',#5596);
#1589=VERTEX_POINT('',#5598);
#1590=VERTEX_POINT('',#5600);
#1591=VERTEX_POINT('',#5602);
#1592=VERTEX_POINT('',#5604);
#1593=VERTEX_POINT('',#5606);
#1594=VERTEX_POINT('',#5608);
#1595=VERTEX_POINT('',#5610);
#1596=VERTEX_POINT('',#5612);
#1597=VERTEX_POINT('',#5615);
#1598=VERTEX_POINT('',#5617);
#1599=VERTEX_POINT('',#5621);
#1600=VERTEX_POINT('',#5625);
#1601=VERTEX_POINT('',#5629);
#1602=VERTEX_POINT('',#5633);
#1603=VERTEX_POINT('',#5634);
#1604=VERTEX_POINT('',#5636);
#1605=VERTEX_POINT('',#5638);
#1606=VERTEX_POINT('',#5640);
#1607=VERTEX_POINT('',#5642);
#1608=VERTEX_POINT('',#5670);
#1609=VERTEX_POINT('',#5671);
#1610=VERTEX_POINT('',#5673);
#1611=VERTEX_POINT('',#5675);
#1612=VERTEX_POINT('',#5677);
#1613=VERTEX_POINT('',#5679);
#1614=VERTEX_POINT('',#5707);
#1615=VERTEX_POINT('',#5719);
#1616=VERTEX_POINT('',#5721);
#1617=VERTEX_POINT('',#5723);
#1618=VERTEX_POINT('',#5725);
#1619=VERTEX_POINT('',#5729);
#1620=VERTEX_POINT('',#5732);
#1621=VERTEX_POINT('',#5736);
#1622=VERTEX_POINT('',#5739);
#1623=VERTEX_POINT('',#5743);
#1624=VERTEX_POINT('',#5746);
#1625=VERTEX_POINT('',#5750);
#1626=VERTEX_POINT('',#5753);
#2004=EDGE_CURVE('',#1585,#1585,#1314,.T.);
#2005=EDGE_CURVE('',#1585,#1586,#863,.T.);
#2006=EDGE_CURVE('',#1586,#1586,#1315,.T.);
#2007=EDGE_CURVE('',#1587,#1588,#1316,.T.);
#2008=EDGE_CURVE('',#1588,#1589,#1317,.T.);
#2009=EDGE_CURVE('',#1589,#1590,#1318,.T.);
#2010=EDGE_CURVE('',#1590,#1591,#864,.T.);
#2011=EDGE_CURVE('',#1592,#1591,#1319,.T.);
#2012=EDGE_CURVE('',#1593,#1592,#1320,.T.);
#2013=EDGE_CURVE('',#1594,#1593,#1321,.T.);
#2014=EDGE_CURVE('',#1595,#1594,#1322,.T.);
#2015=EDGE_CURVE('',#1596,#1595,#1323,.T.);
#2016=EDGE_CURVE('',#1591,#1596,#1324,.T.);
#2017=EDGE_CURVE('',#1590,#1597,#1325,.T.);
#2018=EDGE_CURVE('',#1597,#1598,#1326,.T.);
#2019=EDGE_CURVE('',#1598,#1587,#1327,.T.);
#2020=EDGE_CURVE('',#1599,#1587,#865,.T.);
#2021=EDGE_CURVE('',#1599,#1588,#866,.T.);
#2022=EDGE_CURVE('',#1590,#1600,#867,.T.);
#2023=EDGE_CURVE('',#1600,#1597,#868,.T.);
#2024=EDGE_CURVE('',#1598,#1601,#869,.T.);
#2025=EDGE_CURVE('',#1587,#1601,#870,.T.);
#2026=EDGE_CURVE('',#1602,#1603,#871,.T.);
#2027=EDGE_CURVE('',#1602,#1604,#872,.T.);
#2028=EDGE_CURVE('',#1604,#1605,#873,.T.);
#2029=EDGE_CURVE('',#1605,#1606,#874,.T.);
#2030=EDGE_CURVE('',#1606,#1607,#71,.T.);
#2031=EDGE_CURVE('',#1607,#1603,#875,.T.);
#2032=EDGE_CURVE('',#1608,#1609,#876,.T.);
#2033=EDGE_CURVE('',#1608,#1610,#877,.T.);
#2034=EDGE_CURVE('',#1610,#1611,#878,.T.);
#2035=EDGE_CURVE('',#1611,#1612,#879,.T.);
#2036=EDGE_CURVE('',#1612,#1613,#72,.T.);
#2037=EDGE_CURVE('',#1613,#1609,#880,.T.);
#2038=EDGE_CURVE('',#1589,#1614,#881,.T.);
#2039=EDGE_CURVE('',#1614,#1590,#882,.T.);
#2040=EDGE_CURVE('',#1604,#1608,#1328,.T.);
#2041=EDGE_CURVE('',#1609,#1599,#1329,.T.);
#2042=EDGE_CURVE('',#1601,#1605,#1330,.T.);
#2043=EDGE_CURVE('',#1610,#1602,#1331,.T.);
#2044=EDGE_CURVE('',#1603,#1600,#1332,.T.);
#2045=EDGE_CURVE('',#1614,#1611,#1333,.T.);
#2046=EDGE_CURVE('',#1615,#1596,#883,.T.);
#2047=EDGE_CURVE('',#1596,#1616,#884,.T.);
#2048=EDGE_CURVE('',#1616,#1617,#885,.T.);
#2049=EDGE_CURVE('',#1618,#1617,#886,.T.);
#2050=EDGE_CURVE('',#1615,#1618,#887,.T.);
#2051=EDGE_CURVE('',#1619,#1591,#888,.T.);
#2052=EDGE_CURVE('',#1591,#1615,#889,.T.);
#2053=EDGE_CURVE('',#1620,#1618,#890,.T.);
#2054=EDGE_CURVE('',#1619,#1620,#891,.T.);
#2055=EDGE_CURVE('',#1621,#1592,#892,.T.);
#2056=EDGE_CURVE('',#1592,#1619,#893,.T.);
#2057=EDGE_CURVE('',#1622,#1620,#894,.T.);
#2058=EDGE_CURVE('',#1621,#1622,#895,.T.);
#2059=EDGE_CURVE('',#1623,#1593,#896,.T.);
#2060=EDGE_CURVE('',#1593,#1621,#897,.T.);
#2061=EDGE_CURVE('',#1624,#1622,#898,.T.);
#2062=EDGE_CURVE('',#1623,#1624,#899,.T.);
#2063=EDGE_CURVE('',#1625,#1594,#900,.T.);
#2064=EDGE_CURVE('',#1594,#1623,#901,.T.);
#2065=EDGE_CURVE('',#1626,#1624,#902,.T.);
#2066=EDGE_CURVE('',#1625,#1626,#903,.T.);
#2067=EDGE_CURVE('',#1616,#1595,#904,.T.);
#2068=EDGE_CURVE('',#1595,#1625,#905,.T.);
#2069=EDGE_CURVE('',#1617,#1626,#906,.T.);
#2070=EDGE_CURVE('',#1597,#1607,#1334,.T.);
#2071=EDGE_CURVE('',#1598,#1606,#1335,.T.);
#2072=EDGE_CURVE('',#1612,#1589,#1336,.T.);
#2073=EDGE_CURVE('',#1613,#1588,#1337,.T.);
#2816=ORIENTED_EDGE('',*,*,#2004,.F.);
#2817=ORIENTED_EDGE('',*,*,#2005,.T.);
#2818=ORIENTED_EDGE('',*,*,#2006,.T.);
#2819=ORIENTED_EDGE('',*,*,#2005,.F.);
#2820=ORIENTED_EDGE('',*,*,#2007,.T.);
#2821=ORIENTED_EDGE('',*,*,#2008,.T.);
#2822=ORIENTED_EDGE('',*,*,#2009,.T.);
#2823=ORIENTED_EDGE('',*,*,#2010,.T.);
#2824=ORIENTED_EDGE('',*,*,#2011,.F.);
#2825=ORIENTED_EDGE('',*,*,#2012,.F.);
#2826=ORIENTED_EDGE('',*,*,#2013,.F.);
#2827=ORIENTED_EDGE('',*,*,#2014,.F.);
#2828=ORIENTED_EDGE('',*,*,#2015,.F.);
#2829=ORIENTED_EDGE('',*,*,#2016,.F.);
#2830=ORIENTED_EDGE('',*,*,#2010,.F.);
#2831=ORIENTED_EDGE('',*,*,#2017,.T.);
#2832=ORIENTED_EDGE('',*,*,#2018,.T.);
#2833=ORIENTED_EDGE('',*,*,#2019,.T.);
#2834=ORIENTED_EDGE('',*,*,#2020,.F.);
#2835=ORIENTED_EDGE('',*,*,#2021,.T.);
#2836=ORIENTED_EDGE('',*,*,#2007,.F.);
#2837=ORIENTED_EDGE('',*,*,#2022,.T.);
#2838=ORIENTED_EDGE('',*,*,#2023,.T.);
#2839=ORIENTED_EDGE('',*,*,#2017,.F.);
#2840=ORIENTED_EDGE('',*,*,#2019,.F.);
#2841=ORIENTED_EDGE('',*,*,#2024,.T.);
#2842=ORIENTED_EDGE('',*,*,#2025,.F.);
#2843=ORIENTED_EDGE('',*,*,#2026,.F.);
#2844=ORIENTED_EDGE('',*,*,#2027,.T.);
#2845=ORIENTED_EDGE('',*,*,#2028,.T.);
#2846=ORIENTED_EDGE('',*,*,#2029,.T.);
#2847=ORIENTED_EDGE('',*,*,#2030,.T.);
#2848=ORIENTED_EDGE('',*,*,#2031,.T.);
#2849=ORIENTED_EDGE('',*,*,#2032,.F.);
#2850=ORIENTED_EDGE('',*,*,#2033,.T.);
#2851=ORIENTED_EDGE('',*,*,#2034,.T.);
#2852=ORIENTED_EDGE('',*,*,#2035,.T.);
#2853=ORIENTED_EDGE('',*,*,#2036,.T.);
#2854=ORIENTED_EDGE('',*,*,#2037,.T.);
#2855=ORIENTED_EDGE('',*,*,#2009,.F.);
#2856=ORIENTED_EDGE('',*,*,#2038,.T.);
#2857=ORIENTED_EDGE('',*,*,#2039,.T.);
#2858=ORIENTED_EDGE('',*,*,#2028,.F.);
#2859=ORIENTED_EDGE('',*,*,#2040,.T.);
#2860=ORIENTED_EDGE('',*,*,#2032,.T.);
#2861=ORIENTED_EDGE('',*,*,#2041,.T.);
#2862=ORIENTED_EDGE('',*,*,#2020,.T.);
#2863=ORIENTED_EDGE('',*,*,#2025,.T.);
#2864=ORIENTED_EDGE('',*,*,#2042,.T.);
#2865=ORIENTED_EDGE('',*,*,#2006,.F.);
#2866=ORIENTED_EDGE('',*,*,#2043,.T.);
#2867=ORIENTED_EDGE('',*,*,#2026,.T.);
#2868=ORIENTED_EDGE('',*,*,#2044,.T.);
#2869=ORIENTED_EDGE('',*,*,#2022,.F.);
#2870=ORIENTED_EDGE('',*,*,#2039,.F.);
#2871=ORIENTED_EDGE('',*,*,#2045,.T.);
#2872=ORIENTED_EDGE('',*,*,#2034,.F.);
#2873=ORIENTED_EDGE('',*,*,#2004,.T.);
#2874=ORIENTED_EDGE('',*,*,#2046,.T.);
#2875=ORIENTED_EDGE('',*,*,#2047,.T.);
#2876=ORIENTED_EDGE('',*,*,#2048,.T.);
#2877=ORIENTED_EDGE('',*,*,#2049,.F.);
#2878=ORIENTED_EDGE('',*,*,#2050,.F.);
#2879=ORIENTED_EDGE('',*,*,#2051,.T.);
#2880=ORIENTED_EDGE('',*,*,#2052,.T.);
#2881=ORIENTED_EDGE('',*,*,#2050,.T.);
#2882=ORIENTED_EDGE('',*,*,#2053,.F.);
#2883=ORIENTED_EDGE('',*,*,#2054,.F.);
#2884=ORIENTED_EDGE('',*,*,#2055,.T.);
#2885=ORIENTED_EDGE('',*,*,#2056,.T.);
#2886=ORIENTED_EDGE('',*,*,#2054,.T.);
#2887=ORIENTED_EDGE('',*,*,#2057,.F.);
#2888=ORIENTED_EDGE('',*,*,#2058,.F.);
#2889=ORIENTED_EDGE('',*,*,#2059,.T.);
#2890=ORIENTED_EDGE('',*,*,#2060,.T.);
#2891=ORIENTED_EDGE('',*,*,#2058,.T.);
#2892=ORIENTED_EDGE('',*,*,#2061,.F.);
#2893=ORIENTED_EDGE('',*,*,#2062,.F.);
#2894=ORIENTED_EDGE('',*,*,#2063,.T.);
#2895=ORIENTED_EDGE('',*,*,#2064,.T.);
#2896=ORIENTED_EDGE('',*,*,#2062,.T.);
#2897=ORIENTED_EDGE('',*,*,#2065,.F.);
#2898=ORIENTED_EDGE('',*,*,#2066,.F.);
#2899=ORIENTED_EDGE('',*,*,#2067,.T.);
#2900=ORIENTED_EDGE('',*,*,#2068,.T.);
#2901=ORIENTED_EDGE('',*,*,#2066,.T.);
#2902=ORIENTED_EDGE('',*,*,#2069,.F.);
#2903=ORIENTED_EDGE('',*,*,#2048,.F.);
#2904=ORIENTED_EDGE('',*,*,#2052,.F.);
#2905=ORIENTED_EDGE('',*,*,#2016,.T.);
#2906=ORIENTED_EDGE('',*,*,#2046,.F.);
#2907=ORIENTED_EDGE('',*,*,#2047,.F.);
#2908=ORIENTED_EDGE('',*,*,#2015,.T.);
#2909=ORIENTED_EDGE('',*,*,#2067,.F.);
#2910=ORIENTED_EDGE('',*,*,#2068,.F.);
#2911=ORIENTED_EDGE('',*,*,#2014,.T.);
#2912=ORIENTED_EDGE('',*,*,#2063,.F.);
#2913=ORIENTED_EDGE('',*,*,#2064,.F.);
#2914=ORIENTED_EDGE('',*,*,#2013,.T.);
#2915=ORIENTED_EDGE('',*,*,#2059,.F.);
#2916=ORIENTED_EDGE('',*,*,#2060,.F.);
#2917=ORIENTED_EDGE('',*,*,#2012,.T.);
#2918=ORIENTED_EDGE('',*,*,#2055,.F.);
#2919=ORIENTED_EDGE('',*,*,#2056,.F.);
#2920=ORIENTED_EDGE('',*,*,#2011,.T.);
#2921=ORIENTED_EDGE('',*,*,#2051,.F.);
#2922=ORIENTED_EDGE('',*,*,#2057,.T.);
#2923=ORIENTED_EDGE('',*,*,#2053,.T.);
#2924=ORIENTED_EDGE('',*,*,#2049,.T.);
#2925=ORIENTED_EDGE('',*,*,#2069,.T.);
#2926=ORIENTED_EDGE('',*,*,#2065,.T.);
#2927=ORIENTED_EDGE('',*,*,#2061,.T.);
#2928=ORIENTED_EDGE('',*,*,#2044,.F.);
#2929=ORIENTED_EDGE('',*,*,#2031,.F.);
#2930=ORIENTED_EDGE('',*,*,#2070,.F.);
#2931=ORIENTED_EDGE('',*,*,#2023,.F.);
#2932=ORIENTED_EDGE('',*,*,#2070,.T.);
#2933=ORIENTED_EDGE('',*,*,#2030,.F.);
#2934=ORIENTED_EDGE('',*,*,#2071,.F.);
#2935=ORIENTED_EDGE('',*,*,#2018,.F.);
#2936=ORIENTED_EDGE('',*,*,#2042,.F.);
#2937=ORIENTED_EDGE('',*,*,#2024,.F.);
#2938=ORIENTED_EDGE('',*,*,#2071,.T.);
#2939=ORIENTED_EDGE('',*,*,#2029,.F.);
#2940=ORIENTED_EDGE('',*,*,#2045,.F.);
#2941=ORIENTED_EDGE('',*,*,#2038,.F.);
#2942=ORIENTED_EDGE('',*,*,#2072,.F.);
#2943=ORIENTED_EDGE('',*,*,#2035,.F.);
#2944=ORIENTED_EDGE('',*,*,#2072,.T.);
#2945=ORIENTED_EDGE('',*,*,#2008,.F.);
#2946=ORIENTED_EDGE('',*,*,#2073,.F.);
#2947=ORIENTED_EDGE('',*,*,#2036,.F.);
#2948=ORIENTED_EDGE('',*,*,#2041,.F.);
#2949=ORIENTED_EDGE('',*,*,#2037,.F.);
#2950=ORIENTED_EDGE('',*,*,#2073,.T.);
#2951=ORIENTED_EDGE('',*,*,#2021,.F.);
#2952=ORIENTED_EDGE('',*,*,#2033,.F.);
#2953=ORIENTED_EDGE('',*,*,#2040,.F.);
#2954=ORIENTED_EDGE('',*,*,#2027,.F.);
#2955=ORIENTED_EDGE('',*,*,#2043,.F.);
#3075=CYLINDRICAL_SURFACE('',#3586,2.);
#3076=CYLINDRICAL_SURFACE('',#3589,1.);
#3077=CYLINDRICAL_SURFACE('',#3629,3.);
#3078=CYLINDRICAL_SURFACE('',#3632,3.);
#3079=CYLINDRICAL_SURFACE('',#3633,3.);
#3080=CYLINDRICAL_SURFACE('',#3636,3.);
#3081=CYLINDRICAL_SURFACE('',#3637,3.5);
#3221=ADVANCED_FACE('',(#372),#3075,.F.);
#3222=ADVANCED_FACE('',(#373),#3076,.T.);
#3223=ADVANCED_FACE('',(#374),#212,.F.);
#3224=ADVANCED_FACE('',(#375),#213,.F.);
#3225=ADVANCED_FACE('',(#376),#214,.F.);
#3226=ADVANCED_FACE('',(#377),#215,.T.);
#3227=ADVANCED_FACE('',(#378),#216,.F.);
#3228=ADVANCED_FACE('',(#379),#217,.F.);
#3229=ADVANCED_FACE('',(#380,#131),#218,.T.);
#3230=ADVANCED_FACE('',(#381,#132),#219,.F.);
#3231=ADVANCED_FACE('',(#382),#220,.T.);
#3232=ADVANCED_FACE('',(#383),#221,.T.);
#3233=ADVANCED_FACE('',(#384),#222,.T.);
#3234=ADVANCED_FACE('',(#385),#223,.T.);
#3235=ADVANCED_FACE('',(#386),#224,.T.);
#3236=ADVANCED_FACE('',(#387),#225,.T.);
#3237=ADVANCED_FACE('',(#388),#226,.F.);
#3238=ADVANCED_FACE('',(#389),#227,.F.);
#3239=ADVANCED_FACE('',(#390),#228,.F.);
#3240=ADVANCED_FACE('',(#391),#229,.F.);
#3241=ADVANCED_FACE('',(#392),#230,.F.);
#3242=ADVANCED_FACE('',(#393),#231,.F.);
#3243=ADVANCED_FACE('',(#394),#232,.T.);
#3244=ADVANCED_FACE('',(#395),#3077,.T.);
#3245=ADVANCED_FACE('',(#396),#47,.T.);
#3246=ADVANCED_FACE('',(#397),#3078,.T.);
#3247=ADVANCED_FACE('',(#398),#3079,.T.);
#3248=ADVANCED_FACE('',(#399),#48,.T.);
#3249=ADVANCED_FACE('',(#400),#3080,.T.);
#3250=ADVANCED_FACE('',(#401),#3081,.T.);
#3273=CLOSED_SHELL('',(#3221,#3222,#3223,#3224,#3225,#3226,#3227,#3228,
#3229,#3230,#3231,#3232,#3233,#3234,#3235,#3236,#3237,#3238,#3239,#3240,
#3241,#3242,#3243,#3244,#3245,#3246,#3247,#3248,#3249,#3250));
#3585=AXIS2_PLACEMENT_3D('',#5587,#4388,#4389);
#3586=AXIS2_PLACEMENT_3D('',#5588,#4390,#4391);
#3587=AXIS2_PLACEMENT_3D('',#5590,#4392,#4393);
#3588=AXIS2_PLACEMENT_3D('',#5593,#4395,#4396);
#3589=AXIS2_PLACEMENT_3D('',#5594,#4397,#4398);
#3590=AXIS2_PLACEMENT_3D('',#5597,#4399,#4400);
#3591=AXIS2_PLACEMENT_3D('',#5599,#4401,#4402);
#3592=AXIS2_PLACEMENT_3D('',#5601,#4403,#4404);
#3593=AXIS2_PLACEMENT_3D('',#5605,#4406,#4407);
#3594=AXIS2_PLACEMENT_3D('',#5607,#4408,#4409);
#3595=AXIS2_PLACEMENT_3D('',#5609,#4410,#4411);
#3596=AXIS2_PLACEMENT_3D('',#5611,#4412,#4413);
#3597=AXIS2_PLACEMENT_3D('',#5613,#4414,#4415);
#3598=AXIS2_PLACEMENT_3D('',#5614,#4416,#4417);
#3599=AXIS2_PLACEMENT_3D('',#5616,#4418,#4419);
#3600=AXIS2_PLACEMENT_3D('',#5618,#4420,#4421);
#3601=AXIS2_PLACEMENT_3D('',#5619,#4422,#4423);
#3602=AXIS2_PLACEMENT_3D('',#5620,#4424,#4425);
#3603=AXIS2_PLACEMENT_3D('',#5624,#4428,#4429);
#3604=AXIS2_PLACEMENT_3D('',#5628,#4432,#4433);
#3605=AXIS2_PLACEMENT_3D('',#5632,#4436,#4437);
#3606=AXIS2_PLACEMENT_3D('',#5669,#4443,#4444);
#3607=AXIS2_PLACEMENT_3D('',#5706,#4450,#4451);
#3608=AXIS2_PLACEMENT_3D('',#5710,#4454,#4455);
#3609=AXIS2_PLACEMENT_3D('',#5711,#4456,#4457);
#3610=AXIS2_PLACEMENT_3D('',#5712,#4458,#4459);
#3611=AXIS2_PLACEMENT_3D('',#5713,#4460,#4461);
#3612=AXIS2_PLACEMENT_3D('',#5714,#4462,#4463);
#3613=AXIS2_PLACEMENT_3D('',#5715,#4464,#4465);
#3614=AXIS2_PLACEMENT_3D('',#5716,#4466,#4467);
#3615=AXIS2_PLACEMENT_3D('',#5717,#4468,#4469);
#3616=AXIS2_PLACEMENT_3D('',#5718,#4470,#4471);
#3617=AXIS2_PLACEMENT_3D('',#5728,#4477,#4478);
#3618=AXIS2_PLACEMENT_3D('',#5735,#4483,#4484);
#3619=AXIS2_PLACEMENT_3D('',#5742,#4489,#4490);
#3620=AXIS2_PLACEMENT_3D('',#5749,#4495,#4496);
#3621=AXIS2_PLACEMENT_3D('',#5756,#4501,#4502);
#3622=AXIS2_PLACEMENT_3D('',#5760,#4506,#4507);
#3623=AXIS2_PLACEMENT_3D('',#5761,#4508,#4509);
#3624=AXIS2_PLACEMENT_3D('',#5762,#4510,#4511);
#3625=AXIS2_PLACEMENT_3D('',#5763,#4512,#4513);
#3626=AXIS2_PLACEMENT_3D('',#5764,#4514,#4515);
#3627=AXIS2_PLACEMENT_3D('',#5765,#4516,#4517);
#3628=AXIS2_PLACEMENT_3D('',#5766,#4518,#4519);
#3629=AXIS2_PLACEMENT_3D('',#5767,#4520,#4521);
#3630=AXIS2_PLACEMENT_3D('',#5768,#4522,#4523);
#3631=AXIS2_PLACEMENT_3D('',#5823,#4524,#4525);
#3632=AXIS2_PLACEMENT_3D('',#5824,#4526,#4527);
#3633=AXIS2_PLACEMENT_3D('',#5825,#4528,#4529);
#3634=AXIS2_PLACEMENT_3D('',#5826,#4530,#4531);
#3635=AXIS2_PLACEMENT_3D('',#5881,#4532,#4533);
#3636=AXIS2_PLACEMENT_3D('',#5882,#4534,#4535);
#3637=AXIS2_PLACEMENT_3D('',#5883,#4536,#4537);
#4388=DIRECTION('axis',(0.,0.,1.));
#4389=DIRECTION('refdir',(1.,0.,0.));
#4390=DIRECTION('center_axis',(0.,0.,-1.));
#4391=DIRECTION('ref_axis',(-1.,0.,0.));
#4392=DIRECTION('center_axis',(0.,0.,-1.));
#4393=DIRECTION('ref_axis',(-1.,0.,0.));
#4394=DIRECTION('',(0.,0.,-1.));
#4395=DIRECTION('center_axis',(0.,0.,-1.));
#4396=DIRECTION('ref_axis',(-1.,0.,0.));
#4397=DIRECTION('center_axis',(0.,-1.,0.));
#4398=DIRECTION('ref_axis',(0.,0.,-1.));
#4399=DIRECTION('center_axis',(0.,1.,0.));
#4400=DIRECTION('ref_axis',(0.,0.,1.));
#4401=DIRECTION('center_axis',(0.,1.,0.));
#4402=DIRECTION('ref_axis',(0.,0.,1.));
#4403=DIRECTION('center_axis',(0.,1.,0.));
#4404=DIRECTION('ref_axis',(0.,0.,1.));
#4405=DIRECTION('',(0.,1.,0.));
#4406=DIRECTION('center_axis',(0.,1.,0.));
#4407=DIRECTION('ref_axis',(0.,0.,1.));
#4408=DIRECTION('center_axis',(0.,1.,0.));
#4409=DIRECTION('ref_axis',(0.,0.,1.));
#4410=DIRECTION('center_axis',(0.,1.,0.));
#4411=DIRECTION('ref_axis',(0.,0.,1.));
#4412=DIRECTION('center_axis',(0.,1.,0.));
#4413=DIRECTION('ref_axis',(0.,0.,1.));
#4414=DIRECTION('center_axis',(0.,1.,0.));
#4415=DIRECTION('ref_axis',(0.,0.,1.));
#4416=DIRECTION('center_axis',(0.,1.,0.));
#4417=DIRECTION('ref_axis',(0.,0.,1.));
#4418=DIRECTION('center_axis',(0.,1.,0.));
#4419=DIRECTION('ref_axis',(0.,0.,1.));
#4420=DIRECTION('center_axis',(0.,1.,0.));
#4421=DIRECTION('ref_axis',(0.,0.,1.));
#4422=DIRECTION('center_axis',(0.,1.,0.));
#4423=DIRECTION('ref_axis',(0.,0.,1.));
#4424=DIRECTION('center_axis',(0.,-1.,0.));
#4425=DIRECTION('ref_axis',(0.,0.,-1.));
#4426=DIRECTION('',(1.,0.,0.));
#4427=DIRECTION('',(0.,0.,1.));
#4428=DIRECTION('center_axis',(0.,-1.,0.));
#4429=DIRECTION('ref_axis',(0.,0.,-1.));
#4430=DIRECTION('',(1.,0.,0.));
#4431=DIRECTION('',(0.,0.,-1.));
#4432=DIRECTION('center_axis',(0.,-1.,0.));
#4433=DIRECTION('ref_axis',(0.,0.,-1.));
#4434=DIRECTION('',(0.,0.,-1.));
#4435=DIRECTION('',(1.,0.,0.));
#4436=DIRECTION('center_axis',(1.,0.,0.));
#4437=DIRECTION('ref_axis',(0.,0.,-1.));
#4438=DIRECTION('',(0.,1.,0.));
#4439=DIRECTION('',(0.,0.,-1.));
#4440=DIRECTION('',(0.,1.,0.));
#4441=DIRECTION('',(0.,0.,1.));
#4442=DIRECTION('',(0.,0.,1.));
#4443=DIRECTION('center_axis',(1.,0.,0.));
#4444=DIRECTION('ref_axis',(0.,0.,-1.));
#4445=DIRECTION('',(0.,1.,0.));
#4446=DIRECTION('',(0.,0.,1.));
#4447=DIRECTION('',(0.,1.,0.));
#4448=DIRECTION('',(0.,0.,-1.));
#4449=DIRECTION('',(0.,0.,-1.));
#4450=DIRECTION('center_axis',(0.,-1.,0.));
#4451=DIRECTION('ref_axis',(0.,0.,-1.));
#4452=DIRECTION('',(0.,0.,1.));
#4453=DIRECTION('',(1.,0.,0.));
#4454=DIRECTION('center_axis',(0.,0.,-1.));
#4455=DIRECTION('ref_axis',(-1.,0.,0.));
#4456=DIRECTION('center_axis',(0.,0.,-1.));
#4457=DIRECTION('ref_axis',(-1.,0.,0.));
#4458=DIRECTION('center_axis',(0.,0.,-1.));
#4459=DIRECTION('ref_axis',(-1.,0.,0.));
#4460=DIRECTION('center_axis',(0.,0.,-1.));
#4461=DIRECTION('ref_axis',(-1.,0.,0.));
#4462=DIRECTION('center_axis',(0.,0.,-1.));
#4463=DIRECTION('ref_axis',(-1.,0.,0.));
#4464=DIRECTION('center_axis',(0.,0.,1.));
#4465=DIRECTION('ref_axis',(-1.,0.,0.));
#4466=DIRECTION('center_axis',(0.,0.,1.));
#4467=DIRECTION('ref_axis',(-1.,0.,0.));
#4468=DIRECTION('center_axis',(0.,0.,1.));
#4469=DIRECTION('ref_axis',(-1.,0.,0.));
#4470=DIRECTION('center_axis',(0.866025403784439,0.,0.5));
#4471=DIRECTION('ref_axis',(0.5,0.,-0.866025403784439));
#4472=DIRECTION('',(0.499999999999999,0.,-0.866025403784439));
#4473=DIRECTION('',(0.499999999999999,0.,-0.866025403784439));
#4474=DIRECTION('',(0.,1.,0.));
#4475=DIRECTION('',(0.5,0.,-0.866025403784439));
#4476=DIRECTION('',(0.,1.,0.));
#4477=DIRECTION('center_axis',(2.46473488855316E-16,0.,1.));
#4478=DIRECTION('ref_axis',(1.,0.,-2.46473488855316E-16));
#4479=DIRECTION('',(1.,0.,-2.46473488855316E-16));
#4480=DIRECTION('',(1.,0.,-2.46473488855316E-16));
#4481=DIRECTION('',(1.,0.,-2.46473488855316E-16));
#4482=DIRECTION('',(0.,1.,0.));
#4483=DIRECTION('center_axis',(-0.866025403784438,0.,0.500000000000001));
#4484=DIRECTION('ref_axis',(0.500000000000001,0.,0.866025403784438));
#4485=DIRECTION('',(0.500000000000001,0.,0.866025403784438));
#4486=DIRECTION('',(0.500000000000001,0.,0.866025403784438));
#4487=DIRECTION('',(0.500000000000001,0.,0.866025403784438));
#4488=DIRECTION('',(0.,1.,0.));
#4489=DIRECTION('center_axis',(-0.866025403784439,0.,-0.5));
#4490=DIRECTION('ref_axis',(-0.5,0.,0.866025403784439));
#4491=DIRECTION('',(-0.5,0.,0.866025403784439));
#4492=DIRECTION('',(-0.5,0.,0.866025403784439));
#4493=DIRECTION('',(-0.5,0.,0.866025403784439));
#4494=DIRECTION('',(0.,1.,0.));
#4495=DIRECTION('center_axis',(0.,0.,-1.));
#4496=DIRECTION('ref_axis',(-1.,0.,0.));
#4497=DIRECTION('',(-1.,0.,0.));
#4498=DIRECTION('',(-1.,0.,0.));
#4499=DIRECTION('',(-1.,0.,0.));
#4500=DIRECTION('',(0.,1.,0.));
#4501=DIRECTION('center_axis',(0.866025403784438,0.,-0.500000000000001));
#4502=DIRECTION('ref_axis',(-0.500000000000001,0.,-0.866025403784438));
#4503=DIRECTION('',(-0.500000000000001,0.,-0.866025403784438));
#4504=DIRECTION('',(-0.500000000000001,0.,-0.866025403784438));
#4505=DIRECTION('',(-0.500000000000001,0.,-0.866025403784438));
#4506=DIRECTION('center_axis',(0.,1.,0.));
#4507=DIRECTION('ref_axis',(0.,0.,1.));
#4508=DIRECTION('center_axis',(0.,1.,0.));
#4509=DIRECTION('ref_axis',(0.,0.,1.));
#4510=DIRECTION('center_axis',(0.,1.,0.));
#4511=DIRECTION('ref_axis',(0.,0.,1.));
#4512=DIRECTION('center_axis',(0.,1.,0.));
#4513=DIRECTION('ref_axis',(0.,0.,1.));
#4514=DIRECTION('center_axis',(0.,1.,0.));
#4515=DIRECTION('ref_axis',(0.,0.,1.));
#4516=DIRECTION('center_axis',(0.,1.,0.));
#4517=DIRECTION('ref_axis',(0.,0.,1.));
#4518=DIRECTION('center_axis',(0.,1.,0.));
#4519=DIRECTION('ref_axis',(0.,0.,1.));
#4520=DIRECTION('center_axis',(0.,0.,-1.));
#4521=DIRECTION('ref_axis',(-1.,0.,0.));
#4522=DIRECTION('center_axis',(0.,0.,-1.));
#4523=DIRECTION('ref_axis',(-1.,0.,0.));
#4524=DIRECTION('center_axis',(0.,-1.0842021724855E-16,-1.));
#4525=DIRECTION('ref_axis',(0.,-1.,1.0842021724855E-16));
#4526=DIRECTION('center_axis',(0.,0.,-1.));
#4527=DIRECTION('ref_axis',(-1.,0.,0.));
#4528=DIRECTION('center_axis',(0.,0.,1.));
#4529=DIRECTION('ref_axis',(1.,0.,0.));
#4530=DIRECTION('center_axis',(0.,3.61400724161835E-17,-1.));
#4531=DIRECTION('ref_axis',(0.,1.,3.61400724161835E-17));
#4532=DIRECTION('center_axis',(0.,-5.42101086242747E-16,-1.));
#4533=DIRECTION('ref_axis',(0.,1.,-5.42101086242747E-16));
#4534=DIRECTION('center_axis',(0.,0.,1.));
#4535=DIRECTION('ref_axis',(1.,0.,0.));
#4536=DIRECTION('center_axis',(0.,0.,1.));
#4537=DIRECTION('ref_axis',(1.,0.,0.));
#5587=CARTESIAN_POINT('',(0.,0.,0.));
#5588=CARTESIAN_POINT('Origin',(-16.,-116.5,0.));
#5589=CARTESIAN_POINT('',(-14.,-116.5,0.));
#5590=CARTESIAN_POINT('Origin',(-16.,-116.5,0.));
#5591=CARTESIAN_POINT('',(-14.,-116.5,-2.));
#5592=CARTESIAN_POINT('',(-14.,-116.5,0.));
#5593=CARTESIAN_POINT('Origin',(-16.,-116.5,-2.));
#5594=CARTESIAN_POINT('Origin',(-16.,-60.,-1.));
#5595=CARTESIAN_POINT('',(-16.,-110.,-2.));
#5596=CARTESIAN_POINT('',(-16.5,-110.,-1.86602540378444));
#5597=CARTESIAN_POINT('Origin',(-16.,-110.,-1.));
#5598=CARTESIAN_POINT('',(-16.5,-110.,-0.133974596215562));
#5599=CARTESIAN_POINT('Origin',(-16.,-110.,-1.));
#5600=CARTESIAN_POINT('',(-16.,-110.,-2.16840434497101E-16));
#5601=CARTESIAN_POINT('Origin',(-16.,-110.,-1.));
#5602=CARTESIAN_POINT('',(-16.,-65.,-2.16840434497101E-16));
#5603=CARTESIAN_POINT('',(-16.,-60.,0.));
#5604=CARTESIAN_POINT('',(-16.8660254037844,-65.,-0.499999999999999));
#5605=CARTESIAN_POINT('Origin',(-16.,-65.,-1.));
#5606=CARTESIAN_POINT('',(-16.8660254037844,-65.,-1.5));
#5607=CARTESIAN_POINT('Origin',(-16.,-65.,-1.));
#5608=CARTESIAN_POINT('',(-16.,-65.,-2.));
#5609=CARTESIAN_POINT('Origin',(-16.,-65.,-1.));
#5610=CARTESIAN_POINT('',(-15.1339745962156,-65.,-1.5));
#5611=CARTESIAN_POINT('Origin',(-16.,-65.,-1.));
#5612=CARTESIAN_POINT('',(-15.1339745962156,-65.,-0.500000000000001));
#5613=CARTESIAN_POINT('Origin',(-16.,-65.,-1.));
#5614=CARTESIAN_POINT('Origin',(-16.,-65.,-1.));
#5615=CARTESIAN_POINT('',(-15.5,-110.,-0.133974596215562));
#5616=CARTESIAN_POINT('Origin',(-16.,-110.,-1.));
#5617=CARTESIAN_POINT('',(-15.5,-110.,-1.86602540378444));
#5618=CARTESIAN_POINT('Origin',(-16.,-110.,-1.));
#5619=CARTESIAN_POINT('Origin',(-16.,-110.,-1.));
#5620=CARTESIAN_POINT('Origin',(-19.5,-110.,-2.));
#5621=CARTESIAN_POINT('',(-16.5,-110.,-2.));
#5622=CARTESIAN_POINT('',(-19.5,-110.,-2.));
#5623=CARTESIAN_POINT('',(-16.5,-110.,-2.));
#5624=CARTESIAN_POINT('Origin',(-19.5,-110.,-2.));
#5625=CARTESIAN_POINT('',(-15.5,-110.,0.));
#5626=CARTESIAN_POINT('',(-19.5,-110.,0.));
#5627=CARTESIAN_POINT('',(-15.5,-110.,-2.));
#5628=CARTESIAN_POINT('Origin',(-19.5,-110.,-2.));
#5629=CARTESIAN_POINT('',(-15.5,-110.,-2.));
#5630=CARTESIAN_POINT('',(-15.5,-110.,-2.));
#5631=CARTESIAN_POINT('',(-19.5,-110.,-2.));
#5632=CARTESIAN_POINT('Origin',(-12.5,-120.,-2.));
#5633=CARTESIAN_POINT('',(-12.5,-116.5,0.));
#5634=CARTESIAN_POINT('',(-12.5,-113.,0.));
#5635=CARTESIAN_POINT('',(-12.5,-120.,0.));
#5636=CARTESIAN_POINT('',(-12.5,-116.5,-2.));
#5637=CARTESIAN_POINT('',(-12.5,-116.5,-2.));
#5638=CARTESIAN_POINT('',(-12.5,-113.,-2.));
#5639=CARTESIAN_POINT('',(-12.5,-120.,-2.));
#5640=CARTESIAN_POINT('',(-12.5,-113.,-1.86602540378444));
#5641=CARTESIAN_POINT('',(-12.5,-113.,0.));
#5642=CARTESIAN_POINT('',(-12.5,-113.,-0.133974596215562));
#5643=CARTESIAN_POINT('Ctrl Pts',(-12.5,-113.,-1.86602540378444));
#5644=CARTESIAN_POINT('Ctrl Pts',(-12.5,-112.999999994851,-1.79379309056833));
#5645=CARTESIAN_POINT('Ctrl Pts',(-12.5,-112.998016056892,-1.72157261890518));
#5646=CARTESIAN_POINT('Ctrl Pts',(-12.5,-112.994568071517,-1.64935667749771));
#5647=CARTESIAN_POINT('Ctrl Pts',(-12.5,-112.991126955866,-1.57728461823149));
#5648=CARTESIAN_POINT('Ctrl Pts',(-12.5,-112.986202428167,-1.50521647175664));
#5649=CARTESIAN_POINT('Ctrl Pts',(-12.5,-112.980844807336,-1.43315321107699));
#5650=CARTESIAN_POINT('Ctrl Pts',(-12.5000000000001,-112.975456373403,-1.36067549543516));
#5651=CARTESIAN_POINT('Ctrl Pts',(-12.5000000000004,-112.969634380623,-1.2881978867471));
#5652=CARTESIAN_POINT('Ctrl Pts',(-12.5000000000009,-112.965223416194,-1.21571467716329));
#5653=CARTESIAN_POINT('Ctrl Pts',(-12.5000000000015,-112.960854143347,-1.14391656485544));
#5654=CARTESIAN_POINT('Ctrl Pts',(-12.5000000000017,-112.958046019663,-1.07211583423837));
#5655=CARTESIAN_POINT('Ctrl Pts',(-12.5000000000009,-112.958037668447,-1.00029810032904));
#5656=CARTESIAN_POINT('Ctrl Pts',(-12.5,-112.958029230024,-0.92773041848443));
#5657=CARTESIAN_POINT('Ctrl Pts',(-12.5000000000001,-112.960891052438,-0.855145461004138));
#5658=CARTESIAN_POINT('Ctrl Pts',(-12.5,-112.965330779693,-0.782557921391285));
#5659=CARTESIAN_POINT('Ctrl Pts',(-12.5,-112.969720668615,-0.710785216057982));
#5660=CARTESIAN_POINT('Ctrl Pts',(-12.5,-112.975478101497,-0.639007098038739));
#5661=CARTESIAN_POINT('Ctrl Pts',(-12.5000000000001,-112.980816251273,-0.56722901058433));
#5662=CARTESIAN_POINT('Ctrl Pts',(-12.5000000000001,-112.986204004162,-0.494783947355154));
#5663=CARTESIAN_POINT('Ctrl Pts',(-12.5000000000001,-112.991153168568,-0.422363403854905));
#5664=CARTESIAN_POINT('Ctrl Pts',(-12.5,-112.994603577269,-0.349890285232024));
#5665=CARTESIAN_POINT('Ctrl Pts',(-12.5,-112.998029264397,-0.277936423787971));
#5666=CARTESIAN_POINT('Ctrl Pts',(-12.5,-112.99999999514,-0.206001183885444));
#5667=CARTESIAN_POINT('Ctrl Pts',(-12.5,-113.,-0.133974596215563));
#5668=CARTESIAN_POINT('',(-12.5,-113.,0.));
#5669=CARTESIAN_POINT('Origin',(-19.5,-120.,-2.));
#5670=CARTESIAN_POINT('',(-19.5,-116.5,-2.));
#5671=CARTESIAN_POINT('',(-19.5,-113.,-2.));
#5672=CARTESIAN_POINT('',(-19.5,-120.,-2.));
#5673=CARTESIAN_POINT('',(-19.5,-116.5,0.));
#5674=CARTESIAN_POINT('',(-19.5,-116.5,-2.));
#5675=CARTESIAN_POINT('',(-19.5,-113.,0.));
#5676=CARTESIAN_POINT('',(-19.5,-120.,0.));
#5677=CARTESIAN_POINT('',(-19.5,-113.,-0.133974596215562));
#5678=CARTESIAN_POINT('',(-19.5,-113.,-2.));
#5679=CARTESIAN_POINT('',(-19.5,-113.,-1.86602540378444));
#5680=CARTESIAN_POINT('Ctrl Pts',(-19.5,-113.,-0.133974596215562));
#5681=CARTESIAN_POINT('Ctrl Pts',(-19.5,-112.999999994851,-0.206206909431671));
#5682=CARTESIAN_POINT('Ctrl Pts',(-19.5,-112.998016056892,-0.278427381094817));
#5683=CARTESIAN_POINT('Ctrl Pts',(-19.5,-112.994568071517,-0.350643322502292));
#5684=CARTESIAN_POINT('Ctrl Pts',(-19.5,-112.991126955866,-0.422715381768518));
#5685=CARTESIAN_POINT('Ctrl Pts',(-19.5,-112.986202428167,-0.494783528243354));
#5686=CARTESIAN_POINT('Ctrl Pts',(-19.5,-112.980844807336,-0.566846788923014));
#5687=CARTESIAN_POINT('Ctrl Pts',(-19.5,-112.975456373403,-0.639324504564845));
#5688=CARTESIAN_POINT('Ctrl Pts',(-19.4999999999997,-112.969634380623,-0.711802113252911));
#5689=CARTESIAN_POINT('Ctrl Pts',(-19.4999999999991,-112.965223416194,-0.784285322836707));
#5690=CARTESIAN_POINT('Ctrl Pts',(-19.4999999999986,-112.960854143347,-0.856083435144543));
#5691=CARTESIAN_POINT('Ctrl Pts',(-19.4999999999983,-112.958046019663,-0.927884165761635));
#5692=CARTESIAN_POINT('Ctrl Pts',(-19.4999999999992,-112.958037668447,-0.999701899670956));
#5693=CARTESIAN_POINT('Ctrl Pts',(-19.5,-112.958029230024,-1.07226958151557));
#5694=CARTESIAN_POINT('Ctrl Pts',(-19.5,-112.960891052438,-1.14485453899585));
#5695=CARTESIAN_POINT('Ctrl Pts',(-19.5,-112.965330779693,-1.21744207860871));
#5696=CARTESIAN_POINT('Ctrl Pts',(-19.5,-112.969720668615,-1.28921478394202));
#5697=CARTESIAN_POINT('Ctrl Pts',(-19.5,-112.975478101497,-1.36099290196126));
#5698=CARTESIAN_POINT('Ctrl Pts',(-19.5,-112.980816251273,-1.43277098941567));
#5699=CARTESIAN_POINT('Ctrl Pts',(-19.4999999999999,-112.986204004162,-1.50521605264485));
#5700=CARTESIAN_POINT('Ctrl Pts',(-19.5,-112.991153168568,-1.5776365961451));
#5701=CARTESIAN_POINT('Ctrl Pts',(-19.5,-112.994603577269,-1.65010971476797));
#5702=CARTESIAN_POINT('Ctrl Pts',(-19.5,-112.998029264397,-1.72206357621201));
#5703=CARTESIAN_POINT('Ctrl Pts',(-19.5,-112.99999999514,-1.79399881611456));
#5704=CARTESIAN_POINT('Ctrl Pts',(-19.5,-113.,-1.86602540378443));
#5705=CARTESIAN_POINT('',(-19.5,-113.,-2.));
#5706=CARTESIAN_POINT('Origin',(-19.5,-110.,-2.));
#5707=CARTESIAN_POINT('',(-16.5,-110.,0.));
#5708=CARTESIAN_POINT('',(-16.5,-110.,-2.));
#5709=CARTESIAN_POINT('',(-19.5,-110.,0.));
#5710=CARTESIAN_POINT('Origin',(0.,0.,-2.));
#5711=CARTESIAN_POINT('Origin',(-16.,-116.5,-2.));
#5712=CARTESIAN_POINT('Origin',(-16.5,-113.,-2.));
#5713=CARTESIAN_POINT('Origin',(-15.5,-113.,-2.));
#5714=CARTESIAN_POINT('Origin',(0.,0.,0.));
#5715=CARTESIAN_POINT('Origin',(-16.,-116.5,0.));
#5716=CARTESIAN_POINT('Origin',(-15.5,-113.,0.));
#5717=CARTESIAN_POINT('Origin',(-16.5,-113.,0.));
#5718=CARTESIAN_POINT('Origin',(-15.4226497308104,-65.,-2.98155597433514E-16));
#5719=CARTESIAN_POINT('',(-15.4226497308104,-65.,-2.98155597433514E-16));
#5720=CARTESIAN_POINT('',(-15.4226497308104,-65.,-2.98155597433514E-16));
#5721=CARTESIAN_POINT('',(-14.8452994616208,-65.,-0.999999999999999));
#5722=CARTESIAN_POINT('',(-15.4226497308104,-65.,-2.98155597433514E-16));
#5723=CARTESIAN_POINT('',(-14.8452994616208,-60.,-0.999999999999999));
#5724=CARTESIAN_POINT('',(-14.8452994616208,-65.,-0.999999999999999));
#5725=CARTESIAN_POINT('',(-15.4226497308104,-60.,-2.98155597433514E-16));
#5726=CARTESIAN_POINT('',(-15.4226497308104,-60.,-2.98155597433514E-16));
#5727=CARTESIAN_POINT('',(-15.4226497308104,-65.,-2.98155597433514E-16));
#5728=CARTESIAN_POINT('Origin',(-16.5773502691896,-65.,-1.35525271560688E-17));
#5729=CARTESIAN_POINT('',(-16.5773502691896,-65.,-1.35525271560688E-17));
#5730=CARTESIAN_POINT('',(-16.5773502691896,-65.,-1.35525271560688E-17));
#5731=CARTESIAN_POINT('',(-16.5773502691896,-65.,-1.35525271560688E-17));
#5732=CARTESIAN_POINT('',(-16.5773502691896,-60.,-1.35525271560688E-17));
#5733=CARTESIAN_POINT('',(-16.5773502691896,-60.,-1.35525271560688E-17));
#5734=CARTESIAN_POINT('',(-16.5773502691896,-65.,-1.35525271560688E-17));
#5735=CARTESIAN_POINT('Origin',(-17.1547005383793,-65.,-0.999999999999997));
#5736=CARTESIAN_POINT('',(-17.1547005383793,-65.,-0.999999999999997));
#5737=CARTESIAN_POINT('',(-17.1547005383793,-65.,-0.999999999999997));
#5738=CARTESIAN_POINT('',(-17.1547005383793,-65.,-0.999999999999997));
#5739=CARTESIAN_POINT('',(-17.1547005383793,-60.,-0.999999999999997));
#5740=CARTESIAN_POINT('',(-17.1547005383793,-60.,-0.999999999999997));
#5741=CARTESIAN_POINT('',(-17.1547005383793,-65.,-0.999999999999997));
#5742=CARTESIAN_POINT('Origin',(-16.5773502691896,-65.,-2.));
#5743=CARTESIAN_POINT('',(-16.5773502691896,-65.,-2.));
#5744=CARTESIAN_POINT('',(-16.5773502691896,-65.,-2.));
#5745=CARTESIAN_POINT('',(-16.5773502691896,-65.,-2.));
#5746=CARTESIAN_POINT('',(-16.5773502691896,-60.,-2.));
#5747=CARTESIAN_POINT('',(-16.5773502691896,-60.,-2.));
#5748=CARTESIAN_POINT('',(-16.5773502691896,-65.,-2.));
#5749=CARTESIAN_POINT('Origin',(-15.4226497308104,-65.,-2.));
#5750=CARTESIAN_POINT('',(-15.4226497308104,-65.,-2.));
#5751=CARTESIAN_POINT('',(-15.4226497308104,-65.,-2.));
#5752=CARTESIAN_POINT('',(-15.4226497308104,-65.,-2.));
#5753=CARTESIAN_POINT('',(-15.4226497308104,-60.,-2.));
#5754=CARTESIAN_POINT('',(-15.4226497308104,-60.,-2.));
#5755=CARTESIAN_POINT('',(-15.4226497308104,-65.,-2.));
#5756=CARTESIAN_POINT('Origin',(-14.8452994616208,-65.,-0.999999999999999));
#5757=CARTESIAN_POINT('',(-14.8452994616208,-65.,-0.999999999999999));
#5758=CARTESIAN_POINT('',(-14.8452994616208,-65.,-0.999999999999999));
#5759=CARTESIAN_POINT('',(-14.8452994616208,-60.,-0.999999999999999));
#5760=CARTESIAN_POINT('Origin',(0.,-65.,0.));
#5761=CARTESIAN_POINT('Origin',(0.,-65.,0.));
#5762=CARTESIAN_POINT('Origin',(0.,-65.,0.));
#5763=CARTESIAN_POINT('Origin',(0.,-65.,0.));
#5764=CARTESIAN_POINT('Origin',(0.,-65.,0.));
#5765=CARTESIAN_POINT('Origin',(0.,-65.,0.));
#5766=CARTESIAN_POINT('Origin',(-16.,-60.,-1.));
#5767=CARTESIAN_POINT('Origin',(-15.5,-113.,-2.));
#5768=CARTESIAN_POINT('Origin',(-15.5,-113.,-0.133974596215562));
#5769=CARTESIAN_POINT('Ctrl Pts',(-12.5,-112.998321408359,-0.0215171208906509));
#5770=CARTESIAN_POINT('Ctrl Pts',(-12.5,-109.953990021186,-0.110365484977496));
#5771=CARTESIAN_POINT('Ctrl Pts',(-15.5454993396585,-110.000007198492,-0.108919528903676));
#5772=CARTESIAN_POINT('Ctrl Pts',(-12.5,-113.001650865752,-0.130615518141873));
#5773=CARTESIAN_POINT('Ctrl Pts',(-12.5,-109.994846910505,-0.129517847817374));
#5774=CARTESIAN_POINT('Ctrl Pts',(-15.5052244365464,-110.000000774232,-0.130950785426593));
#5775=CARTESIAN_POINT('Ctrl Pts',(-12.5,-112.999829763877,-0.240121651459518));
#5776=CARTESIAN_POINT('Ctrl Pts',(-12.5,-110.044590565554,-0.157043650297362));
#5777=CARTESIAN_POINT('Ctrl Pts',(-15.4555037853853,-109.999992849754,-0.157582174193049));
#5778=CARTESIAN_POINT('Ctrl Pts',(-12.5,-112.991171615148,-0.421989183009334));
#5779=CARTESIAN_POINT('Ctrl Pts',(-12.5,-110.144230037263,-0.248024746671439));
#5780=CARTESIAN_POINT('Ctrl Pts',(-15.3483339572922,-109.999976541827,-0.239998260254286));
#5781=CARTESIAN_POINT('Ctrl Pts',(-12.5,-112.986249389692,-0.494130629734298));
#5782=CARTESIAN_POINT('Ctrl Pts',(-12.5,-110.187949454441,-0.295175701491007));
#5783=CARTESIAN_POINT('Ctrl Pts',(-15.299011567492,-109.999969217678,-0.282541606351056));
#5784=CARTESIAN_POINT('Ctrl Pts',(-12.5,-112.975531858613,-0.638340025483971));
#5785=CARTESIAN_POINT('Ctrl Pts',(-12.5,-110.278138535025,-0.42781535733713));
#5786=CARTESIAN_POINT('Ctrl Pts',(-15.1911611365941,-109.999953678584,-0.406847658471516));
#5787=CARTESIAN_POINT('Ctrl Pts',(-12.5,-112.969742052832,-0.710437616206344));
#5788=CARTESIAN_POINT('Ctrl Pts',(-12.5,-110.324934754411,-0.513809199029964));
#5789=CARTESIAN_POINT('Ctrl Pts',(-15.1317804589651,-109.999945443368,-0.489955254864159));
#5790=CARTESIAN_POINT('Ctrl Pts',(-12.5,-112.960920191473,-0.854678268466455));
#5791=CARTESIAN_POINT('Ctrl Pts',(-12.5,-110.397592333861,-0.731264401632342));
#5792=CARTESIAN_POINT('Ctrl Pts',(-15.0350207661438,-109.999932251101,-0.712428738528866));
#5793=CARTESIAN_POINT('Ctrl Pts',(-12.5,-112.95806404802,-0.926824230509072));
#5794=CARTESIAN_POINT('Ctrl Pts',(-12.5000000000005,-110.422001594761,-0.864088334522592));
#5795=CARTESIAN_POINT('Ctrl Pts',(-15.0007136147036,-109.999927765103,-0.853647804036836));
#5796=CARTESIAN_POINT('Ctrl Pts',(-12.5,-112.958016061818,-1.07120954970003));
#5797=CARTESIAN_POINT('Ctrl Pts',(-12.4999999999996,-110.422406145868,-1.13224899582074));
#5798=CARTESIAN_POINT('Ctrl Pts',(-15.0001457739159,-109.999927689389,-1.14241971794702));
#5799=CARTESIAN_POINT('Ctrl Pts',(-12.5,-112.960828724944,-1.14344898114294));
#5800=CARTESIAN_POINT('Ctrl Pts',(-12.4999999999999,-110.398355492936,-1.26557410071784));
#5801=CARTESIAN_POINT('Ctrl Pts',(-15.0339698860841,-109.999932110923,-1.28425554920314));
#5802=CARTESIAN_POINT('Ctrl Pts',(-12.5,-112.969622749834,-1.28798009071552));
#5803=CARTESIAN_POINT('Ctrl Pts',(-12.5000000000001,-110.325910420761,-1.48413970176802));
#5804=CARTESIAN_POINT('Ctrl Pts',(-15.1305184541349,-109.999945269335,-1.50802137948635));
#5805=CARTESIAN_POINT('Ctrl Pts',(-12.5,-112.97542425227,-1.36026880325738));
#5806=CARTESIAN_POINT('Ctrl Pts',(-12.5,-110.279014567801,-1.57069480005754));
#5807=CARTESIAN_POINT('Ctrl Pts',(-15.1900769619304,-109.999953525122,-1.5917262456063));
#5808=CARTESIAN_POINT('Ctrl Pts',(-12.5,-112.986176452745,-1.50483219996039));
#5809=CARTESIAN_POINT('Ctrl Pts',(-12.5,-110.188587950114,-1.70408671874064));
#5810=CARTESIAN_POINT('Ctrl Pts',(-15.2982789162811,-109.999969109764,-1.71678752331027));
#5811=CARTESIAN_POINT('Ctrl Pts',(-12.5,-112.991118555997,-1.57710674240752));
#5812=CARTESIAN_POINT('Ctrl Pts',(-12.4999999999996,-110.144750106835,-1.75144466546231));
#5813=CARTESIAN_POINT('Ctrl Pts',(-15.3477573301302,-109.999976455226,-1.75952009740825));
#5814=CARTESIAN_POINT('Ctrl Pts',(-12.5,-112.999819986014,-1.75935530906393));
#5815=CARTESIAN_POINT('Ctrl Pts',(-12.5000000000006,-110.044829996224,-1.84282328506315));
#5816=CARTESIAN_POINT('Ctrl Pts',(-15.455261801624,-109.999992811267,-1.84228939912907));
#5817=CARTESIAN_POINT('Ctrl Pts',(-12.5,-113.001670882596,-1.86929829726474));
#5818=CARTESIAN_POINT('Ctrl Pts',(-12.5000000000052,-109.994838487951,-1.87052042344478));
#5819=CARTESIAN_POINT('Ctrl Pts',(-15.5052368990814,-110.000000775553,-1.86906791930568));
#5820=CARTESIAN_POINT('Ctrl Pts',(-12.5,-112.998303161317,-1.97915370173891));
#5821=CARTESIAN_POINT('Ctrl Pts',(-12.4999999999913,-109.953739602693,-1.88974229707348));
#5822=CARTESIAN_POINT('Ctrl Pts',(-15.5457412933844,-110.000007237571,-1.89120504794152));
#5823=CARTESIAN_POINT('Origin',(-15.5,-113.,-1.86602540378444));
#5824=CARTESIAN_POINT('Origin',(-15.5,-113.,-2.));
#5825=CARTESIAN_POINT('Origin',(-16.5,-113.,-2.));
#5826=CARTESIAN_POINT('Origin',(-16.5,-113.,-0.133974596215562));
#5827=CARTESIAN_POINT('Ctrl Pts',(-19.5,-112.998321408359,-1.97848287910703));
#5828=CARTESIAN_POINT('Ctrl Pts',(-19.5,-109.953990021188,-1.88963451502302));
#5829=CARTESIAN_POINT('Ctrl Pts',(-16.4545006603424,-110.000007198492,-1.89108047109586));
#5830=CARTESIAN_POINT('Ctrl Pts',(-19.5,-113.001650865752,-1.86938448185662));
#5831=CARTESIAN_POINT('Ctrl Pts',(-19.5,-109.994846910506,-1.87048215218166));
#5832=CARTESIAN_POINT('Ctrl Pts',(-16.4947755634543,-110.000000774232,-1.86904921457304));
#5833=CARTESIAN_POINT('Ctrl Pts',(-19.5,-112.999829763877,-1.7598783485397));
#5834=CARTESIAN_POINT('Ctrl Pts',(-19.5,-110.044590565554,-1.84295634970223));
#5835=CARTESIAN_POINT('Ctrl Pts',(-16.5444962146153,-109.999992849754,-1.84241782580659));
#5836=CARTESIAN_POINT('Ctrl Pts',(-19.5,-112.991171615148,-1.57801081699067));
#5837=CARTESIAN_POINT('Ctrl Pts',(-19.5,-110.144230037263,-1.75197525332857));
#5838=CARTESIAN_POINT('Ctrl Pts',(-16.6516660427078,-109.999976541827,-1.76000173974572));
#5839=CARTESIAN_POINT('Ctrl Pts',(-19.5,-112.986249389692,-1.5058693702657));
#5840=CARTESIAN_POINT('Ctrl Pts',(-19.5,-110.187949454441,-1.70482429850909));
#5841=CARTESIAN_POINT('Ctrl Pts',(-16.7009884325079,-109.999969217678,-1.71745839364903));
#5842=CARTESIAN_POINT('Ctrl Pts',(-19.5,-112.975531858613,-1.36165997451602));
#5843=CARTESIAN_POINT('Ctrl Pts',(-19.5,-110.278138535025,-1.57218464266277));
#5844=CARTESIAN_POINT('Ctrl Pts',(-16.8088388634061,-109.999953678584,-1.59315234152839));
#5845=CARTESIAN_POINT('Ctrl Pts',(-19.5,-112.969742052832,-1.28956238379365));
#5846=CARTESIAN_POINT('Ctrl Pts',(-19.5,-110.324934754411,-1.48619080097002));
#5847=CARTESIAN_POINT('Ctrl Pts',(-16.868219541035,-109.999945443368,-1.51004474513582));
#5848=CARTESIAN_POINT('Ctrl Pts',(-19.5,-112.960920191473,-1.14532173153354));
#5849=CARTESIAN_POINT('Ctrl Pts',(-19.5,-110.397592333861,-1.26873559836766));
#5850=CARTESIAN_POINT('Ctrl Pts',(-16.9649792338562,-109.999932251101,-1.28757126147114));
#5851=CARTESIAN_POINT('Ctrl Pts',(-19.5,-112.95806404802,-1.07317576949094));
#5852=CARTESIAN_POINT('Ctrl Pts',(-19.4999999999996,-110.422001594761,-1.13591166547741));
#5853=CARTESIAN_POINT('Ctrl Pts',(-16.9992863852965,-109.999927765103,-1.14635219596316));
#5854=CARTESIAN_POINT('Ctrl Pts',(-19.5,-112.958016061818,-0.928790450299966));
#5855=CARTESIAN_POINT('Ctrl Pts',(-19.5000000000004,-110.422406145868,-0.867751004179269));
#5856=CARTESIAN_POINT('Ctrl Pts',(-16.9998542260842,-109.999927689389,-0.857580282052989));
#5857=CARTESIAN_POINT('Ctrl Pts',(-19.5,-112.960828724944,-0.856551018857039));
#5858=CARTESIAN_POINT('Ctrl Pts',(-19.5,-110.398355492936,-0.734425899282093));
#5859=CARTESIAN_POINT('Ctrl Pts',(-16.9660301139158,-109.999932110923,-0.715744450796804));
#5860=CARTESIAN_POINT('Ctrl Pts',(-19.5,-112.969622749834,-0.712019909284494));
#5861=CARTESIAN_POINT('Ctrl Pts',(-19.5,-110.325910420762,-0.515860298232045));
#5862=CARTESIAN_POINT('Ctrl Pts',(-16.8694815458653,-109.999945269335,-0.491978620513704));
#5863=CARTESIAN_POINT('Ctrl Pts',(-19.5,-112.97542425227,-0.63973119674263));
#5864=CARTESIAN_POINT('Ctrl Pts',(-19.5000000000001,-110.279014567801,-0.429305199942497));
#5865=CARTESIAN_POINT('Ctrl Pts',(-16.8099230380697,-109.999953525122,-0.408273754393743));
#5866=CARTESIAN_POINT('Ctrl Pts',(-19.5,-112.986176452745,-0.495167800039601));
#5867=CARTESIAN_POINT('Ctrl Pts',(-19.4999999999999,-110.188587950114,-0.295913281259317));
#5868=CARTESIAN_POINT('Ctrl Pts',(-16.7017210837189,-109.999969109764,-0.283212476689676));
#5869=CARTESIAN_POINT('Ctrl Pts',(-19.5,-112.991118555997,-0.422893257592481));
#5870=CARTESIAN_POINT('Ctrl Pts',(-19.5000000000005,-110.144750106835,-0.248555334537643));
#5871=CARTESIAN_POINT('Ctrl Pts',(-16.6522426698697,-109.999976455226,-0.240479902591688));
#5872=CARTESIAN_POINT('Ctrl Pts',(-19.5,-112.999819986014,-0.240644690936843));
#5873=CARTESIAN_POINT('Ctrl Pts',(-19.4999999999992,-110.044829996224,-0.157176714937319));
#5874=CARTESIAN_POINT('Ctrl Pts',(-16.5447381983765,-109.999992811267,-0.157710600871371));
#5875=CARTESIAN_POINT('Ctrl Pts',(-19.5,-113.001670882596,-0.130701702736794));
#5876=CARTESIAN_POINT('Ctrl Pts',(-19.499999999995,-109.994838487952,-0.129479576555088));
#5877=CARTESIAN_POINT('Ctrl Pts',(-16.4947631009191,-110.000000775553,-0.130932080694481));
#5878=CARTESIAN_POINT('Ctrl Pts',(-19.5,-112.998303161317,-0.0208462982633885));
#5879=CARTESIAN_POINT('Ctrl Pts',(-19.5000000000085,-109.953739602694,-0.11025770292768));
#5880=CARTESIAN_POINT('Ctrl Pts',(-16.4542587066167,-110.000007237571,-0.108794952059203));
#5881=CARTESIAN_POINT('Origin',(-16.5,-113.,-1.86602540378444));
#5882=CARTESIAN_POINT('Origin',(-16.5,-113.,-2.));
#5883=CARTESIAN_POINT('Origin',(-16.,-116.5,-2.));
#5978=UNCERTAINTY_MEASURE_WITH_UNIT(LENGTH_MEASURE(0.01),#5991,
'DISTANCE_ACCURACY_VALUE',
'Maximum model space distance between geometric entities at asserted c
onnectivities');
#5981=UNCERTAINTY_MEASURE_WITH_UNIT(LENGTH_MEASURE(0.01),#5991,
'DISTANCE_ACCURACY_VALUE',
'Maximum model space distance between geometric entities at asserted c
onnectivities');
#5987=(
GEOMETRIC_REPRESENTATION_CONTEXT(3)
GLOBAL_UNCERTAINTY_ASSIGNED_CONTEXT((#5978))
GLOBAL_UNIT_ASSIGNED_CONTEXT((#5991,#5993,#5994))
REPRESENTATION_CONTEXT('','3D')
);
#5990=(
GEOMETRIC_REPRESENTATION_CONTEXT(3)
GLOBAL_UNCERTAINTY_ASSIGNED_CONTEXT((#5981))
GLOBAL_UNIT_ASSIGNED_CONTEXT((#5991,#5993,#5994))
REPRESENTATION_CONTEXT('','3D')
);
#5991=(
LENGTH_UNIT()
NAMED_UNIT(*)
SI_UNIT(.MILLI.,.METRE.)
);
#5993=(
NAMED_UNIT(*)
PLANE_ANGLE_UNIT()
SI_UNIT($,.RADIAN.)
);
#5994=(
NAMED_UNIT(*)
SI_UNIT($,.STERADIAN.)
SOLID_ANGLE_UNIT()
);
#6000=SHAPE_DEFINITION_REPRESENTATION(#6008,#6025);
#6008=PRODUCT_DEFINITION_SHAPE('',$,#6034);
#6025=SHAPE_REPRESENTATION('',(#3585),#5987);
#6028=PRODUCT_DEFINITION_CONTEXT('part definition',#6054,'design');
#6034=PRODUCT_DEFINITION('screw driver','screw driver',#6042,#6028);
#6042=PRODUCT_DEFINITION_FORMATION('',$,#6061);
#6054=APPLICATION_CONTEXT(
'Core Data for Automotive Mechanical Design Process');
#6055=PRODUCT_CONTEXT('part definition',#6054,'mechanical');
#6061=PRODUCT('screw driver','screw driver',$,(#6055));
#6067=PRESENTATION_STYLE_ASSIGNMENT((#6073));
#6073=SURFACE_STYLE_USAGE(.BOTH.,#6079);
#6079=SURFACE_SIDE_STYLE('',(#6085));
#6085=SURFACE_STYLE_FILL_AREA(#6091);
#6091=FILL_AREA_STYLE('Opaque(31,36,43)',(#6097));
#6097=FILL_AREA_STYLE_COLOUR('Opaque(31,36,43)',#6103);
#6103=COLOUR_RGB('Opaque(31,36,43)',0.12156862745098,0.141176470588235,
0.168627450980392);
ENDSEC;
END-ISO-10303-21;
